ISO-10303-21;
HEADER;
FILE_DESCRIPTION (('STEP AP203'),
    '1' );
FILE_NAME ('1602p_c_16.step',
    '2026-10-31T14:11:27',
    ( '' ),
    ( '' ),
    'SwSTEP 2.0',
    'SolidWorks 2024',
    '' );
FILE_SCHEMA (( 'AUTOMOTIVE_DESIGN' ));
ENDSEC;

DATA;
#42=DIRECTION ( 'NONE',  ( 2.269747459788994803E-13, 2.220446049250620342E-15, 1.000000000000000000 ) ) ;
#160=CARTESIAN_POINT ( 'NONE',  ( -20.00000000397459843, 22.95208919257349933, -7.999999999995569766 ) ) ;
#191=ORIENTED_EDGE ( 'NONE', *, *, #19640, .F. ) ;
#236=EDGE_CURVE ( 'NONE', #10293, #10039, #18795, .T. ) ;
#273=DIRECTION ( 'NONE',  ( 2.269747459788990007E-13, 2.220446049250330436E-15, 1.000000000000000000 ) ) ;
#337=DIRECTION ( 'NONE',  ( -2.269747459788994803E-13, -2.220446049250715400E-15, -1.000000000000000000 ) ) ;
#415=DIRECTION ( 'NONE',  ( 1.000000000000000000, 0.000000000000000000, 0.000000000000000000 ) ) ;
#449=EDGE_CURVE ( 'NONE', #23261, #20507, #13870, .T. ) ;
#490=LINE ( 'NONE', #2631, #20485 ) ;
#501=SHAPE_DEFINITION_REPRESENTATION ( #22718, #9605 ) ;
#590=ORIENTED_EDGE ( 'NONE', *, *, #8239, .F. ) ;
#647=DIRECTION ( 'NONE',  ( 2.269747459788994803E-13, 2.220446049250715400E-15, 1.000000000000000000 ) ) ;
#698=ORIENTED_EDGE ( 'NONE', *, *, #20723, .T. ) ;
#782=EDGE_CURVE ( 'NONE', #8934, #14619, #17447, .T. ) ;
#787=ORIENTED_EDGE ( 'NONE', *, *, #5363, .F. ) ;
#831=DIRECTION ( 'NONE',  ( 9.248903203239929993E-11, -1.000000000000000000, 2.220446028257650359E-15 ) ) ;
#874=PLANE ( 'NONE',  #17305 ) ;
#1002=DIRECTION ( 'NONE',  ( 2.269747459788994803E-13, 2.220446049250330436E-15, 1.000000000000000000 ) ) ;
#1011=LINE ( 'NONE', #15045, #7252 ) ;
#1092=DIRECTION ( 'NONE',  ( -1.000000000000000000, -6.662112528310618598E-09, 2.269018306577664942E-13 ) ) ;
#1126=DIRECTION ( 'NONE',  ( -1.000000000000000000, -6.662112528310618598E-09, 2.269018306577664942E-13 ) ) ;
#1138=VERTEX_POINT ( 'NONE', #22231 ) ;
#1142=VERTEX_POINT ( 'NONE', #5976 ) ;
#1161=DIRECTION ( 'NONE',  ( 2.269747459788999852E-13, 2.220446049250325308E-15, 1.000000000000000000 ) ) ;
#1241=CIRCLE ( 'NONE', #13381, 2.499999999999998668 ) ;
#1253=AXIS2_PLACEMENT_3D ( 'NONE', #17483, #4779, #22937 ) ;
#1287=DIRECTION ( 'NONE',  ( 1.000000000000000000, -2.099275139236451291E-23, -2.269747374248204951E-13 ) ) ;
#1415=AXIS2_PLACEMENT_3D ( 'NONE', #1710, #23433, #3374 ) ;
#1420=ORIENTED_EDGE ( 'NONE', *, *, #5020, .F. ) ;
#1462=VERTEX_POINT ( 'NONE', #17383 ) ;
#1495=AXIS2_PLACEMENT_3D ( 'NONE', #9711, #647, #14917 ) ;
#1507=ORIENTED_EDGE ( 'NONE', *, *, #7243, .F. ) ;
#1517=ORIENTED_EDGE ( 'NONE', *, *, #9574, .F. ) ;
#1518=ORIENTED_EDGE ( 'NONE', *, *, #13071, .F. ) ;
#1576=UNCERTAINTY_MEASURE_WITH_UNIT (LENGTH_MEASURE( 1.000000000000000082E-05 ), #9687, 'distance_accuracy_value', 'NONE');
#1595=EDGE_CURVE ( 'NONE', #17959, #4383, #18222, .T. ) ;
#1625=DIRECTION ( 'NONE',  ( -1.000000000000000000, -6.662112528310618598E-09, 2.269018306577664942E-13 ) ) ;
#1710=CARTESIAN_POINT ( 'NONE',  ( -12.59661859123080063, -1.225550774622850225, -7.999999999997189803 ) ) ;
#1734=( GEOMETRIC_REPRESENTATION_CONTEXT ( 3 ) GLOBAL_UNCERTAINTY_ASSIGNED_CONTEXT ( ( #1576 ) ) GLOBAL_UNIT_ASSIGNED_CONTEXT ( ( #9687, #15004, #7886 ) ) REPRESENTATION_CONTEXT ( 'NONE', 'WORKASPACE' ) );
#1739=VERTEX_POINT ( 'NONE', #21751 ) ;
#1769=ORIENTED_EDGE ( 'NONE', *, *, #22920, .F. ) ;
#1787=MECHANICAL_CONTEXT ( 'NONE', #12343, 'mechanical' ) ;
#1797=VECTOR ( 'NONE', #6698, 1000.000000000000000 ) ;
#1813=DIRECTION ( 'NONE',  ( -0.8823529412199823119, 0.4705882352125332901, 1.992040791580033901E-13 ) ) ;
#1855=ORIENTED_EDGE ( 'NONE', *, *, #8239, .T. ) ;
#1891=FACE_OUTER_BOUND ( 'NONE', #16050, .T. ) ;
#1926=PLANE ( 'NONE',  #6182 ) ;
#1948=AXIS2_PLACEMENT_3D ( 'NONE', #15826, #23055, #18078 ) ;
#2021=CIRCLE ( 'NONE', #19477, 5.999999999999999112 ) ;
#2036=VECTOR ( 'NONE', #21744, 1000.000000000000000 ) ;
#2049=VECTOR ( 'NONE', #9440, 1000.000000000000000 ) ;
#2068=CARTESIAN_POINT ( 'NONE',  ( -27.50000000434419789, 26.95208919188010199, -6.749999999993870681 ) ) ;
#2130=ORIENTED_EDGE ( 'NONE', *, *, #9185, .F. ) ;
#2133=ORIENTED_EDGE ( 'NONE', *, *, #10985, .T. ) ;
#2172=ORIENTED_EDGE ( 'NONE', *, *, #11346, .F. ) ;
#2214=ADVANCED_FACE ( 'NONE', ( #18409 ), #9135, .T. ) ;
#2313=AXIS2_PLACEMENT_3D ( 'NONE', #14663, #20127, #16322 ) ;
#2336=DIRECTION ( 'NONE',  ( 1.000000000000000000, 6.662111938308250026E-09, -2.269747459936919981E-13 ) ) ;
#2372=DIRECTION ( 'NONE',  ( -1.000000000000000000, -6.662112528310618598E-09, 2.269018306577664942E-13 ) ) ;
#2392=VECTOR ( 'NONE', #21709, 1000.000000000000000 ) ;
#2437=CARTESIAN_POINT ( 'NONE',  ( -14.00000000202700079, 1.899127378930349996, -6.749999999996879829 ) ) ;
#2451=DIRECTION ( 'NONE',  ( 0.7806762821593219437, -0.6249356306643899517, -1.759009604640482394E-13 ) ) ;
#2478=ORIENTED_EDGE ( 'NONE', *, *, #17643, .F. ) ;
#2515=CARTESIAN_POINT ( 'NONE',  ( -14.00000000202730099, 1.899127378930349996, -7.999999999996879829 ) ) ;
#2547=ADVANCED_FACE ( 'NONE', ( #15124, #13010, #4445 ), #874, .F. ) ;
#2552=EDGE_LOOP ( 'NONE', ( #3963, #3451, #20173, #11611 ) ) ;
#2569=CARTESIAN_POINT ( 'NONE',  ( 0.000000000000000000, 0.000000000000000000, 0.000000000000000000 ) ) ;
#2576=EDGE_CURVE ( 'NONE', #22163, #22602, #10894, .T. ) ;
#2611=CARTESIAN_POINT ( 'NONE',  ( -27.50000000434449987, 26.95208919188010199, -7.999999999993869793 ) ) ;
#2612=VECTOR ( 'NONE', #831, 1000.000000000000000 ) ;
#2631=CARTESIAN_POINT ( 'NONE',  ( -14.70588235717659842, 25.77561860482770228, -6.749999999996769695 ) ) ;
#2672=DIRECTION ( 'NONE',  ( 2.269747459788994803E-13, 2.220446049250715400E-15, 1.000000000000000000 ) ) ;
#2780=CIRCLE ( 'NONE', #17186, 5.999999999999999112 ) ;
#2832=PRODUCT ( '1602p_c_16', '1602p_c_16', '', ( #1787 ) ) ;
#2864=CARTESIAN_POINT ( 'NONE',  ( -26.00000000397469790, 22.95208919201850151, -7.999999999994199307 ) ) ;
#2935=ORIENTED_EDGE ( 'NONE', *, *, #1595, .T. ) ;
#2944=FACE_BOUND ( 'NONE', #9645, .T. ) ;
#2989=VERTEX_POINT ( 'NONE', #12973 ) ;
#3038=DESIGN_CONTEXT ( 'detailed design', #7768, 'design' ) ;
#3078=DIRECTION ( 'NONE',  ( -1.000000000000000000, -6.662112528310618598E-09, 2.269018306577664942E-13 ) ) ;
#3101=CARTESIAN_POINT ( 'NONE',  ( -25.29411765129429668, 25.77561860384869874, -6.749999999994369837 ) ) ;
#3117=CARTESIAN_POINT ( 'NONE',  ( -26.00000000397409750, 22.95208919201850151, -5.499999999994199307 ) ) ;
#3123=DIRECTION ( 'NONE',  ( 2.269747459788999852E-13, 2.220446049250325308E-15, 1.000000000000000000 ) ) ;
#3219=DIRECTION ( 'NONE',  ( 2.269747459789000104E-13, 2.220446049250330436E-15, 1.000000000000000000 ) ) ;
#3332=VERTEX_POINT ( 'NONE', #9010 ) ;
#3366=VECTOR ( 'NONE', #22037, 1000.000000000000000 ) ;
#3374=DIRECTION ( 'NONE',  ( 0.7806762821592939661, -0.6249356306644247017, -1.755540157688528527E-13 ) ) ;
#3385=ORIENTED_EDGE ( 'NONE', *, *, #2576, .T. ) ;
#3451=ORIENTED_EDGE ( 'NONE', *, *, #6935, .F. ) ;
#3487=DIRECTION ( 'NONE',  ( -1.000000000000000000, -9.248903203239929993E-11, 2.269747459791049881E-13 ) ) ;
#3536=CIRCLE ( 'NONE', #19094, 2.500000000000001776 ) ;
#3543=AXIS2_PLACEMENT_3D ( 'NONE', #21318, #1002, #10187 ) ;
#3580=EDGE_LOOP ( 'NONE', ( #2935, #10284 ) ) ;
#3592=EDGE_CURVE ( 'NONE', #13456, #12123, #1011, .T. ) ;
#3628=DIRECTION ( 'NONE',  ( 2.269747459788990007E-13, 2.220446049250330436E-15, 1.000000000000000000 ) ) ;
#3649=ORIENTED_EDGE ( 'NONE', *, *, #3592, .F. ) ;
#3660=ORIENTED_EDGE ( 'NONE', *, *, #8984, .T. ) ;
#3731=DIRECTION ( 'NONE',  ( 1.000000000000000000, 9.249025156865542385E-11, -2.269596547736322531E-13 ) ) ;
#3767=ORIENTED_EDGE ( 'NONE', *, *, #18292, .F. ) ;
#3805=ADVANCED_FACE ( 'NONE', ( #7092 ), #12673, .T. ) ;
#3861=CARTESIAN_POINT ( 'NONE',  ( -22.52506283708739687, 28.95208917575130414, -6.749999999995010214 ) ) ;
#3900=DIRECTION ( 'NONE',  ( -1.000000000000000000, -6.662112528310618598E-09, 2.269018306577664942E-13 ) ) ;
#3902=VECTOR ( 'NONE', #10466, 1000.000000000000000 ) ;
#3935=DIRECTION ( 'NONE',  ( 2.269747459788999852E-13, 2.220446049250325308E-15, 1.000000000000000000 ) ) ;
#3939=CIRCLE ( 'NONE', #11570, 6.000000000000000000 ) ;
#3946=DIRECTION ( 'NONE',  ( 2.269747459789000104E-13, 2.220446049250330436E-15, 1.000000000000000000 ) ) ;
#3963=ORIENTED_EDGE ( 'NONE', *, *, #12184, .T. ) ;
#3972=LINE ( 'NONE', #19286, #21396 ) ;
#3974=DIRECTION ( 'NONE',  ( 5.039851780001396616E-28, 2.220446049301850153E-15, 1.000000000000000000 ) ) ;
#4113=VECTOR ( 'NONE', #2336, 1000.000000000000000 ) ;
#4210=DIRECTION ( 'NONE',  ( -0.8823529412199658806, 0.4705882352125641543, 1.991462550421374292E-13 ) ) ;
#4338=CIRCLE ( 'NONE', #17612, 2.499999999999998668 ) ;
#4372=ORIENTED_EDGE ( 'NONE', *, *, #4721, .T. ) ;
#4383=VERTEX_POINT ( 'NONE', #19884 ) ;
#4437=CARTESIAN_POINT ( 'NONE',  ( -20.00000000397459843, 22.95208919257349933, -7.999999999995569766 ) ) ;
#4445=FACE_OUTER_BOUND ( 'NONE', #23098, .T. ) ;
#4455=CARTESIAN_POINT ( 'NONE',  ( -17.47493719149800029, 26.45208920939580111, -5.499999999996139977 ) ) ;
#4460=CYLINDRICAL_SURFACE ( 'NONE', #7686, 2.500000000000000000 ) ;
#4507=ORIENTED_EDGE ( 'NONE', *, *, #449, .T. ) ;
#4551=CARTESIAN_POINT ( 'NONE',  ( -17.47493719149830227, 26.45208920939580111, -6.749999999996139977 ) ) ;
#4569=ORIENTED_EDGE ( 'NONE', *, *, #10985, .F. ) ;
#4611=FACE_OUTER_BOUND ( 'NONE', #23393, .T. ) ;
#4655=CIRCLE ( 'NONE', #7685, 2.500000000000000444 ) ;
#4704=AXIS2_PLACEMENT_3D ( 'NONE', #2611, #20772, #20888 ) ;
#4721=EDGE_CURVE ( 'NONE', #2989, #1142, #21043, .T. ) ;
#4779=DIRECTION ( 'NONE',  ( 2.269747459788990007E-13, 2.220446049250330436E-15, 1.000000000000000000 ) ) ;
#4819=FACE_OUTER_BOUND ( 'NONE', #15318, .T. ) ;
#4843=DIRECTION ( 'NONE',  ( 2.269747459788990007E-13, 2.220446049250330436E-15, 1.000000000000000000 ) ) ;
#4862=CARTESIAN_POINT ( 'NONE',  ( -20.00000000000130029, -20.00000000000000000, -5.499999999995469402 ) ) ;
#4870=EDGE_CURVE ( 'NONE', #22602, #23272, #9634, .T. ) ;
#4906=EDGE_CURVE ( 'NONE', #20851, #10381, #16390, .T. ) ;
#4911=CARTESIAN_POINT ( 'NONE',  ( -14.00000000000180123, -19.99999999944489915, -7.999999999996829203 ) ) ;
#4963=CARTESIAN_POINT ( 'NONE',  ( -20.00000000000130029, -20.00000000000000000, -5.499999999995469402 ) ) ;
#4968=DIRECTION ( 'NONE',  ( 0.000000000000000000, 1.000000000000000000, -9.248937406224699144E-11 ) ) ;
#5020=EDGE_CURVE ( 'NONE', #23452, #16466, #7964, .T. ) ;
#5059=AXIS2_PLACEMENT_3D ( 'NONE', #4963, #21007, #1625 ) ;
#5061=CARTESIAN_POINT ( 'NONE',  ( -20.00000000000140332, -20.00000000000000000, -5.499999999995469402 ) ) ;
#5206=CARTESIAN_POINT ( 'NONE',  ( -12.59661859123020022, -1.225550774622840233, -5.499999999997189803 ) ) ;
#5223=EDGE_CURVE ( 'NONE', #16864, #8907, #9884, .T. ) ;
#5309=LINE ( 'NONE', #11030, #3366 ) ;
#5313=PLANE ( 'NONE',  #16355 ) ;
#5315=ORIENTED_EDGE ( 'NONE', *, *, #13319, .T. ) ;
#5339=ORIENTED_EDGE ( 'NONE', *, *, #16091, .T. ) ;
#5340=ORIENTED_EDGE ( 'NONE', *, *, #22749, .T. ) ;
#5358=FACE_OUTER_BOUND ( 'NONE', #12719, .T. ) ;
#5363=EDGE_CURVE ( 'NONE', #12123, #23452, #14437, .T. ) ;
#5404=CARTESIAN_POINT ( 'NONE',  ( -20.00000000397430000, 22.95208919257349933, -6.749999999995570654 ) ) ;
#5414=ADVANCED_BREP_SHAPE_REPRESENTATION ( '', ( #9367, #12739 ), #1734 ) ;
#5458=ADVANCED_FACE ( 'NONE', ( #5885 ), #14913, .T. ) ;
#5499=LINE ( 'NONE', #9298, #23386 ) ;
#5524=CARTESIAN_POINT ( 'NONE',  ( -17.50000000397430000, 22.95208920922877738, -6.749999999996137312 ) ) ;
#5548=ORIENTED_EDGE ( 'NONE', *, *, #12930, .T. ) ;
#5575=CARTESIAN_POINT ( 'NONE',  ( -20.00000000397430000, 22.95208919257349933, -6.749999999995570654 ) ) ;
#5658=ORIENTED_EDGE ( 'NONE', *, *, #21355, .F. ) ;
#5722=LINE ( 'NONE', #7753, #22457 ) ;
#5769=AXIS2_PLACEMENT_3D ( 'NONE', #14319, #18014, #19906 ) ;
#5814=DIRECTION ( 'NONE',  ( 1.000000000000000000, -2.099364410518905248E-23, -2.269747374240930013E-13 ) ) ;
#5851=AXIS2_PLACEMENT_3D ( 'NONE', #2068, #42, #16210 ) ;
#5859=ORIENTED_EDGE ( 'NONE', *, *, #16091, .F. ) ;
#5885=FACE_OUTER_BOUND ( 'NONE', #12387, .T. ) ;
#5905=DIRECTION ( 'NONE',  ( 2.269747459789000104E-13, 2.220446049250330436E-15, 1.000000000000000000 ) ) ;
#5922=DIRECTION ( 'NONE',  ( -2.269747459788994803E-13, -2.220446049250330436E-15, -1.000000000000000000 ) ) ;
#5941=VERTEX_POINT ( 'NONE', #9189 ) ;
#5976=CARTESIAN_POINT ( 'NONE',  ( -14.54830929633950021, -2.787889851644880235, -5.499999999996740385 ) ) ;
#5983=SHAPE_REPRESENTATION_RELATIONSHIP ( 'NONE' , 'NONE' ,  #9605, #5414 ) ;
#6037=DIRECTION ( 'NONE',  ( 1.000000000000000000, 9.250482324585361611E-11, -2.269018306577663175E-13 ) ) ;
#6182=AXIS2_PLACEMENT_3D ( 'NONE', #21876, #3487, #9306 ) ;
#6342=LINE ( 'NONE', #4911, #21484 ) ;
#6434=EDGE_CURVE ( 'NONE', #1138, #12006, #16508, .T. ) ;
#6473=CARTESIAN_POINT ( 'NONE',  ( -25.29411765129399825, 25.77561860384869874, -5.499999999994369837 ) ) ;
#6645=CARTESIAN_POINT ( 'NONE',  ( -20.00479999606179859, 1.846597379377909798, -5.499999999995520028 ) ) ;
#6656=DIRECTION ( 'NONE',  ( 0.7806762821592939661, -0.6249356306644249237, -1.759009604640482141E-13 ) ) ;
#6679=ORIENTED_EDGE ( 'NONE', *, *, #21355, .T. ) ;
#6698=DIRECTION ( 'NONE',  ( -9.248903203239929993E-11, 1.000000000000000000, -2.220446028257650359E-15 ) ) ;
#6735=DIRECTION ( 'NONE',  ( 2.269747459788990007E-13, 2.220446049250330436E-15, 1.000000000000000000 ) ) ;
#6746=ORIENTED_EDGE ( 'NONE', *, *, #5020, .T. ) ;
#6803=DIRECTION ( 'NONE',  ( 2.269747459788994803E-13, 2.220446049250470459E-15, 1.000000000000000000 ) ) ;
#6823=CARTESIAN_POINT ( 'NONE',  ( -12.59661859123050043, -1.225550774622850225, -6.749999999997189803 ) ) ;
#6935=EDGE_CURVE ( 'NONE', #19931, #15954, #16020, .T. ) ;
#6940=AXIS2_PLACEMENT_3D ( 'NONE', #4455, #18944, #20833 ) ;
#6962=AXIS2_PLACEMENT_3D ( 'NONE', #11348, #13341, #22471 ) ;
#7033=ORIENTED_EDGE ( 'NONE', *, *, #18675, .F. ) ;
#7067=EDGE_CURVE ( 'NONE', #22148, #13627, #1241, .T. ) ;
#7071=FACE_OUTER_BOUND ( 'NONE', #19559, .T. ) ;
#7077=ORIENTED_EDGE ( 'NONE', *, *, #782, .T. ) ;
#7092=FACE_OUTER_BOUND ( 'NONE', #21578, .T. ) ;
#7128=ORIENTED_EDGE ( 'NONE', *, *, #8356, .T. ) ;
#7130=VECTOR ( 'NONE', #3219, 1000.000000000000000 ) ;
#7243=EDGE_CURVE ( 'NONE', #19931, #3332, #14159, .T. ) ;
#7252=VECTOR ( 'NONE', #8046, 1000.000000000000000 ) ;
#7406=AXIS2_PLACEMENT_3D ( 'NONE', #20320, #3935, #11209 ) ;
#7420=AXIS2_PLACEMENT_3D ( 'NONE', #13987, #4843, #17681 ) ;
#7522=CARTESIAN_POINT ( 'NONE',  ( -26.00000000000149925, -20.00000000055539928, -5.499999999994109601 ) ) ;
#7585=CARTESIAN_POINT ( 'NONE',  ( -14.00000000397430000, 22.95208919312840123, -6.749999999996930455 ) ) ;
#7594=ORIENTED_EDGE ( 'NONE', *, *, #12184, .F. ) ;
#7655=DIRECTION ( 'NONE',  ( 1.000000000000000000, -2.269747459789000104E-13, -7.174648137343060814E-44 ) ) ;
#7685=AXIS2_PLACEMENT_3D ( 'NONE', #19787, #14435, #12552 ) ;
#7686=AXIS2_PLACEMENT_3D ( 'NONE', #22255, #2672, #2451 ) ;
#7744=DIRECTION ( 'NONE',  ( 2.269747459789000104E-13, 2.220446049250330436E-15, 1.000000000000000000 ) ) ;
#7753=CARTESIAN_POINT ( 'NONE',  ( -17.47493720815390006, 28.95208920939580111, -7.999999999996148858 ) ) ;
#7761=ORIENTED_EDGE ( 'NONE', *, *, #18976, .F. ) ;
#7768=APPLICATION_CONTEXT ( 'configuration controlled 3d designs of mechanical parts and assemblies' ) ;
#7817=CARTESIAN_POINT ( 'NONE',  ( -12.50000000434420144, 26.95208919326699970, -6.749999999997279510 ) ) ;
#7835=EDGE_LOOP ( 'NONE', ( #5340, #12149, #18160, #8254 ) ) ;
#7877=EDGE_LOOP ( 'NONE', ( #20407, #11366 ) ) ;
#7886=( NAMED_UNIT ( * ) SI_UNIT ( $, .STERADIAN. ) SOLID_ANGLE_UNIT ( ) );
#7964=CIRCLE ( 'NONE', #21221, 2.500000000000000000 ) ;
#8046=DIRECTION ( 'NONE',  ( 2.269747459789000104E-13, 2.220446049250330436E-15, 1.000000000000000000 ) ) ;
#8082=CARTESIAN_POINT ( 'NONE',  ( -22.52506282043209751, 26.45208917575140006, -6.749999999994999555 ) ) ;
#8125=ORIENTED_EDGE ( 'NONE', *, *, #13319, .F. ) ;
#8133=CYLINDRICAL_SURFACE ( 'NONE', #18909, 2.500000000000000444 ) ;
#8138=AXIS2_PLACEMENT_3D ( 'NONE', #5206, #17445, #6656 ) ;
#8167=LINE ( 'NONE', #18762, #23260 ) ;
#8239=EDGE_CURVE ( 'NONE', #8907, #16864, #17201, .T. ) ;
#8254=ORIENTED_EDGE ( 'NONE', *, *, #6935, .T. ) ;
#8274=CARTESIAN_POINT ( 'NONE',  ( -14.00000000397399980, 22.95208919312840123, -5.499999999996930455 ) ) ;
#8356=EDGE_CURVE ( 'NONE', #16192, #20851, #22887, .T. ) ;
#8391=DIRECTION ( 'NONE',  ( 2.269747459788990007E-13, 2.220446049250330436E-15, 1.000000000000000000 ) ) ;
#8416=FACE_BOUND ( 'NONE', #3580, .T. ) ;
#8496=DIRECTION ( 'NONE',  ( 0.7806762821592939661, -0.6249356306644247017, -1.759009604640482141E-13 ) ) ;
#8525=CYLINDRICAL_SURFACE ( 'NONE', #14705, 2.499999999999998668 ) ;
#8528=VERTEX_POINT ( 'NONE', #18261 ) ;
#8543=CARTESIAN_POINT ( 'NONE',  ( -22.52506283708709844, 28.95208917575130414, -5.499999999995009325 ) ) ;
#8598=DIRECTION ( 'NONE',  ( 2.269747459789000104E-13, 2.220446049250330436E-15, 1.000000000000000000 ) ) ;
#8612=CARTESIAN_POINT ( 'NONE',  ( -17.47493720815390006, 28.95208920939580111, -7.999999999996148858 ) ) ;
#8651=DIRECTION ( 'NONE',  ( 2.269747459788990007E-13, 2.220446049250330436E-15, 1.000000000000000000 ) ) ;
#8797=ADVANCED_FACE ( 'NONE', ( #4819 ), #12428, .F. ) ;
#8907=VERTEX_POINT ( 'NONE', #20009 ) ;
#8934=VERTEX_POINT ( 'NONE', #16437 ) ;
#8965=AXIS2_PLACEMENT_3D ( 'NONE', #7585, #5814, #16256 ) ;
#8978=ADVANCED_FACE ( 'NONE', ( #18359 ), #11126, .F. ) ;
#8984=EDGE_CURVE ( 'NONE', #11278, #5941, #4338, .T. ) ;
#9010=CARTESIAN_POINT ( 'NONE',  ( -14.00000000000180123, -19.99999999944489915, -7.999999999996829203 ) ) ;
#9135=PLANE ( 'NONE',  #8965 ) ;
#9144=ORIENTED_EDGE ( 'NONE', *, *, #13435, .T. ) ;
#9149=DIRECTION ( 'NONE',  ( 2.269747459788990007E-13, 2.220446049250330436E-15, 1.000000000000000000 ) ) ;
#9185=EDGE_CURVE ( 'NONE', #14619, #23452, #14894, .T. ) ;
#9189=CARTESIAN_POINT ( 'NONE',  ( -17.50000000397459843, 22.95208920922877738, -7.999999999996137312 ) ) ;
#9198=CIRCLE ( 'NONE', #6940, 2.500000000000000444 ) ;
#9252=ORIENTED_EDGE ( 'NONE', *, *, #18675, .T. ) ;
#9255=ORIENTED_EDGE ( 'NONE', *, *, #19640, .T. ) ;
#9260=EDGE_CURVE ( 'NONE', #1739, #1462, #3972, .T. ) ;
#9278=EDGE_LOOP ( 'NONE', ( #20192, #3649, #23424, #15052 ) ) ;
#9298=CARTESIAN_POINT ( 'NONE',  ( -22.50000000000149925, -20.00000001665528160, -6.749999999994902744 ) ) ;
#9306=DIRECTION ( 'NONE',  ( -9.248903203239929993E-11, 1.000000000000000000, 0.000000000000000000 ) ) ;
#9321=DIRECTION ( 'NONE',  ( 2.269747459788994803E-13, 2.220446049250330436E-15, 1.000000000000000000 ) ) ;
#9325=LINE ( 'NONE', #5524, #11922 ) ;
#9355=VECTOR ( 'NONE', #22090, 1000.000000000000000 ) ;
#9367=MANIFOLD_SOLID_BREP ( 'Imported1', #22698 ) ;
#9440=DIRECTION ( 'NONE',  ( 2.269747459789000104E-13, 2.220446049250330436E-15, 1.000000000000000000 ) ) ;
#9488=VECTOR ( 'NONE', #20068, 1000.000000000000000 ) ;
#9491=CARTESIAN_POINT ( 'NONE',  ( -16.50000000144870071, -4.350228928667009498, -5.499999999996299849 ) ) ;
#9574=EDGE_CURVE ( 'NONE', #16192, #18788, #490, .T. ) ;
#9605=SHAPE_REPRESENTATION ( '1602p_c_16', ( #12739 ), #1734 ) ;
#9634=CIRCLE ( 'NONE', #23108, 2.499999999999998668 ) ;
#9645=EDGE_LOOP ( 'NONE', ( #1855, #15293 ) ) ;
#9687=( LENGTH_UNIT ( ) NAMED_UNIT ( * ) SI_UNIT ( .MILLI., .METRE. ) );
#9711=CARTESIAN_POINT ( 'NONE',  ( -16.50000000202729922, 1.899127378699190016, -7.999999999996308730 ) ) ;
#9779=CIRCLE ( 'NONE', #1415, 2.500000000000000444 ) ;
#9781=CARTESIAN_POINT ( 'NONE',  ( -14.70588235717680092, 25.77561860482770228, -7.999999999996769695 ) ) ;
#9806=CARTESIAN_POINT ( 'NONE',  ( -27.50000000434389946, 26.95208919188010199, -5.499999999993869793 ) ) ;
#9884=CIRCLE ( 'NONE', #21236, 2.499999999999998668 ) ;
#9958=AXIS2_PLACEMENT_3D ( 'NONE', #6823, #10166, #8496 ) ;
#9988=EDGE_CURVE ( 'NONE', #10039, #22602, #22039, .T. ) ;
#10039=VERTEX_POINT ( 'NONE', #15915 ) ;
#10093=PLANE ( 'NONE',  #22946 ) ;
#10166=DIRECTION ( 'NONE',  ( 2.269747459788999852E-13, 2.220446049250475192E-15, 1.000000000000000000 ) ) ;
#10168=ORIENTED_EDGE ( 'NONE', *, *, #4906, .T. ) ;
#10179=AXIS2_PLACEMENT_3D ( 'NONE', #4437, #13933, #1092 ) ;
#10186=VECTOR ( 'NONE', #10207, 1000.000000000000000 ) ;
#10187=DIRECTION ( 'NONE',  ( -1.000000000000000000, -9.259491321837100239E-11, 2.269596547736281384E-13 ) ) ;
#10193=ORIENTED_EDGE ( 'NONE', *, *, #5223, .F. ) ;
#10207=DIRECTION ( 'NONE',  ( -2.269747459789000104E-13, -2.220446049250330436E-15, -1.000000000000000000 ) ) ;
#10258=ORIENTED_EDGE ( 'NONE', *, *, #18976, .T. ) ;
#10284=ORIENTED_EDGE ( 'NONE', *, *, #22177, .T. ) ;
#10293=VERTEX_POINT ( 'NONE', #16102 ) ;
#10305=CARTESIAN_POINT ( 'NONE',  ( -20.00000000000149925, -20.00000000000000000, -6.749999999995469402 ) ) ;
#10331=LINE ( 'NONE', #21349, #17662 ) ;
#10381=VERTEX_POINT ( 'NONE', #15634 ) ;
#10465=CARTESIAN_POINT ( 'NONE',  ( -22.50000000397400157, 22.95208917591821773, -5.499999999995003108 ) ) ;
#10466=DIRECTION ( 'NONE',  ( 2.269747459789000104E-13, 2.220446049250330436E-15, 1.000000000000000000 ) ) ;
#10531=EDGE_CURVE ( 'NONE', #13456, #16192, #22785, .T. ) ;
#10627=CARTESIAN_POINT ( 'NONE',  ( -25.29411765129449918, 25.77561860384869874, -7.999999999994368949 ) ) ;
#10635=DIRECTION ( 'NONE',  ( -9.249330715586770885E-11, 1.000000000000000000, -2.220446028256680454E-15 ) ) ;
#10697=ORIENTED_EDGE ( 'NONE', *, *, #17837, .F. ) ;
#10784=CYLINDRICAL_SURFACE ( 'NONE', #15850, 6.000000000000000000 ) ;
#10837=VERTEX_POINT ( 'NONE', #10627 ) ;
#10894=CIRCLE ( 'NONE', #14660, 2.500000000000000444 ) ;
#10918=CARTESIAN_POINT ( 'NONE',  ( -14.00000000202680006, 1.899127378930359988, -5.499999999996879829 ) ) ;
#10960=EDGE_LOOP ( 'NONE', ( #3660, #22470 ) ) ;
#10985=EDGE_CURVE ( 'NONE', #13627, #8907, #5499, .T. ) ;
#11030=CARTESIAN_POINT ( 'NONE',  ( -22.52506283708739687, 28.95208917575130414, -6.749999999995010214 ) ) ;
#11068=ORIENTED_EDGE ( 'NONE', *, *, #20723, .F. ) ;
#11086=CARTESIAN_POINT ( 'NONE',  ( -14.54830929662869998, 0.3367883020382160253, -6.749999999996750155 ) ) ;
#11126=CYLINDRICAL_SURFACE ( 'NONE', #5851, 2.500000000000000444 ) ;
#11209=DIRECTION ( 'NONE',  ( -6.662112528310618598E-09, 1.000000000000000000, -2.081668171172169697E-15 ) ) ;
#11257=EDGE_CURVE ( 'NONE', #10837, #22163, #15920, .T. ) ;
#11278=VERTEX_POINT ( 'NONE', #15700 ) ;
#11291=ORIENTED_EDGE ( 'NONE', *, *, #12930, .F. ) ;
#11310=CYLINDRICAL_SURFACE ( 'NONE', #15311, 2.499999999999998668 ) ;
#11346=EDGE_CURVE ( 'NONE', #20851, #20507, #18122, .T. ) ;
#11348=CARTESIAN_POINT ( 'NONE',  ( -16.50000000144900270, -4.350228928667009498, -6.749999999996299849 ) ) ;
#11361=CARTESIAN_POINT ( 'NONE',  ( -20.00479999606239900, 1.846597379377900028, -7.999999999995519140 ) ) ;
#11366=ORIENTED_EDGE ( 'NONE', *, *, #7067, .T. ) ;
#11428=VECTOR ( 'NONE', #5905, 1000.000000000000000 ) ;
#11436=CARTESIAN_POINT ( 'NONE',  ( -22.50000000397430000, 22.95208917591821773, -6.749999999995003108 ) ) ;
#11534=CARTESIAN_POINT ( 'NONE',  ( -20.00000000000180123, -20.00000000000000000, -7.999999999995469402 ) ) ;
#11537=CIRCLE ( 'NONE', #1253, 2.499999999999998668 ) ;
#11570=AXIS2_PLACEMENT_3D ( 'NONE', #21949, #12943, #14836 ) ;
#11611=ORIENTED_EDGE ( 'NONE', *, *, #16961, .T. ) ;
#11689=AXIS2_PLACEMENT_3D ( 'NONE', #15267, #18954, #13722 ) ;
#11717=DIRECTION ( 'NONE',  ( 2.269747459788994803E-13, 2.220446049250605354E-15, 1.000000000000000000 ) ) ;
#11731=CARTESIAN_POINT ( 'NONE',  ( -17.50000000000180123, -19.99999998334472195, -7.999999999996036060 ) ) ;
#11846=ADVANCED_FACE ( 'NONE', ( #20771 ), #17444, .T. ) ;
#11855=CARTESIAN_POINT ( 'NONE',  ( -20.00000000000149925, -20.00000000000000000, -6.749999999995469402 ) ) ;
#11856=PRODUCT_DEFINITION_FORMATION_WITH_SPECIFIED_SOURCE ( 'ANY', '', #2832, .NOT_KNOWN. ) ;
#11884=DIRECTION ( 'NONE',  ( 1.000000000000000000, -2.269747459789000104E-13, -7.174648137343060814E-44 ) ) ;
#11922=VECTOR ( 'NONE', #3628, 1000.000000000000000 ) ;
#11943=EDGE_LOOP ( 'NONE', ( #6746, #11291, #7077, #14092 ) ) ;
#11982=ORIENTED_EDGE ( 'NONE', *, *, #4870, .F. ) ;
#12006=VERTEX_POINT ( 'NONE', #18749 ) ;
#12011=CARTESIAN_POINT ( 'NONE',  ( -17.50000000000130029, -19.99999998334472195, -5.499999999996036948 ) ) ;
#12013=ORIENTED_EDGE ( 'NONE', *, *, #236, .T. ) ;
#12109=CARTESIAN_POINT ( 'NONE',  ( -17.47493720815359808, 28.95208920939580111, -6.749999999996149747 ) ) ;
#12113=CARTESIAN_POINT ( 'NONE',  ( -12.50000000434450165, 26.95208919326699970, -7.999999999997280398 ) ) ;
#12123=VERTEX_POINT ( 'NONE', #8274 ) ;
#12149=ORIENTED_EDGE ( 'NONE', *, *, #9260, .F. ) ;
#12184=EDGE_CURVE ( 'NONE', #8528, #15954, #18505, .T. ) ;
#12275=ORIENTED_EDGE ( 'NONE', *, *, #22296, .F. ) ;
#12282=DIRECTION ( 'NONE',  ( -0.8823529412199823119, 0.4705882352125332901, 1.992040791580033901E-13 ) ) ;
#12343=APPLICATION_CONTEXT ( 'configuration controlled 3d designs of mechanical parts and assemblies' ) ;
#12387=EDGE_LOOP ( 'NONE', ( #9144, #4507, #5339, #5315 ) ) ;
#12428=CYLINDRICAL_SURFACE ( 'NONE', #23268, 2.499999999999998668 ) ;
#12460=LINE ( 'NONE', #2864, #2612 ) ;
#12552=DIRECTION ( 'NONE',  ( 1.000000000000000000, 9.250482324585361611E-11, -2.269018306577663175E-13 ) ) ;
#12586=EDGE_CURVE ( 'NONE', #5941, #11278, #20391, .T. ) ;
#12619=ADVANCED_FACE ( 'NONE', ( #20820 ), #8133, .T. ) ;
#12673=CYLINDRICAL_SURFACE ( 'NONE', #5769, 5.999999999999999112 ) ;
#12719=EDGE_LOOP ( 'NONE', ( #698, #1517, #7128, #10168 ) ) ;
#12739=AXIS2_PLACEMENT_3D ( 'NONE', #2569, #13380, #415 ) ;
#12813=CARTESIAN_POINT ( 'NONE',  ( -26.00000000000179767, -20.00000000055539928, -6.749999999994109601 ) ) ;
#12834=CARTESIAN_POINT ( 'NONE',  ( -22.52506282043179908, 26.45208917575140006, -5.499999999994999555 ) ) ;
#12930=EDGE_CURVE ( 'NONE', #8934, #16466, #14746, .T. ) ;
#12943=DIRECTION ( 'NONE',  ( -2.269747459788994803E-13, -2.220446049250330436E-15, -1.000000000000000000 ) ) ;
#12973=CARTESIAN_POINT ( 'NONE',  ( -14.54830929634010062, -2.787889851644890005, -7.999999999996738609 ) ) ;
#13005=DIRECTION ( 'NONE',  ( -1.000000000000000000, -6.662112528310618598E-09, 2.269018306577664942E-13 ) ) ;
#13010=FACE_BOUND ( 'NONE', #10960, .T. ) ;
#13060=ORIENTED_EDGE ( 'NONE', *, *, #6434, .T. ) ;
#13071=EDGE_CURVE ( 'NONE', #1739, #19931, #12460, .T. ) ;
#13319=EDGE_CURVE ( 'NONE', #10293, #23272, #5309, .T. ) ;
#13341=DIRECTION ( 'NONE',  ( 2.269747459788994803E-13, 2.220446049250330436E-15, 1.000000000000000000 ) ) ;
#13370=VECTOR ( 'NONE', #10635, 1000.000000000000000 ) ;
#13380=DIRECTION ( 'NONE',  ( 0.000000000000000000, 0.000000000000000000, 1.000000000000000000 ) ) ;
#13381=AXIS2_PLACEMENT_3D ( 'NONE', #11534, #16955, #3900 ) ;
#13395=EDGE_LOOP ( 'NONE', ( #19491, #8125, #12013, #21904 ) ) ;
#13435=EDGE_CURVE ( 'NONE', #23272, #23261, #20734, .T. ) ;
#13456=VERTEX_POINT ( 'NONE', #17185 ) ;
#13487=ORIENTED_EDGE ( 'NONE', *, *, #23264, .T. ) ;
#13551=AXIS2_PLACEMENT_3D ( 'NONE', #13912, #19153, #15451 ) ;
#13627=VERTEX_POINT ( 'NONE', #14082 ) ;
#13634=DIRECTION ( 'NONE',  ( 5.039851780001396616E-28, 2.220446049301850153E-15, 1.000000000000000000 ) ) ;
#13696=ADVANCED_FACE ( 'NONE', ( #17418 ), #8525, .F. ) ;
#13722=DIRECTION ( 'NONE',  ( -1.000000000000000000, -6.662112528310618598E-09, 2.269018306577664942E-13 ) ) ;
#13784=ADVANCED_FACE ( 'NONE', ( #19777 ), #10784, .T. ) ;
#13804=ORIENTED_EDGE ( 'NONE', *, *, #2576, .F. ) ;
#13816=ORIENTED_EDGE ( 'NONE', *, *, #11257, .T. ) ;
#13854=ORIENTED_EDGE ( 'NONE', *, *, #1595, .F. ) ;
#13870=LINE ( 'NONE', #12109, #10186 ) ;
#13881=ORIENTED_EDGE ( 'NONE', *, *, #10531, .F. ) ;
#13912=CARTESIAN_POINT ( 'NONE',  ( -17.47493719149860070, 26.45208920939580111, -7.999999999996139088 ) ) ;
#13933=DIRECTION ( 'NONE',  ( 2.269747459788990007E-13, 2.220446049250330436E-15, 1.000000000000000000 ) ) ;
#13962=DIRECTION ( 'NONE',  ( -1.000000000000000000, -9.259491321837100239E-11, 2.269596547736281384E-13 ) ) ;
#13987=CARTESIAN_POINT ( 'NONE',  ( -20.00000000397430000, 22.95208919257349933, -6.749999999995570654 ) ) ;
#13993=CARTESIAN_POINT ( 'NONE',  ( -14.00000000144900092, -4.350228928435750042, -6.749999999996870059 ) ) ;
#14031=DIRECTION ( 'NONE',  ( 2.269747459789000104E-13, 2.220446049250330436E-15, 1.000000000000000000 ) ) ;
#14082=CARTESIAN_POINT ( 'NONE',  ( -22.50000000000180123, -20.00000001665528160, -7.999999999994901856 ) ) ;
#14092=ORIENTED_EDGE ( 'NONE', *, *, #9185, .T. ) ;
#14159=CIRCLE ( 'NONE', #3543, 6.000000000000109246 ) ;
#14164=EDGE_CURVE ( 'NONE', #3332, #1138, #6342, .T. ) ;
#14167=AXIS2_PLACEMENT_3D ( 'NONE', #22364, #22807, #20257 ) ;
#14199=CIRCLE ( 'NONE', #8138, 2.500000000000000444 ) ;
#14235=LINE ( 'NONE', #20574, #3902 ) ;
#14319=CARTESIAN_POINT ( 'NONE',  ( -20.00000000397430000, 22.95208919257349933, -6.749999999995570654 ) ) ;
#14398=DIRECTION ( 'NONE',  ( 2.269747459788990007E-13, 2.220446049250330436E-15, 1.000000000000000000 ) ) ;
#14435=DIRECTION ( 'NONE',  ( 2.269747459788994803E-13, 2.220446049250330436E-15, 1.000000000000000000 ) ) ;
#14437=LINE ( 'NONE', #22022, #20870 ) ;
#14498=DIRECTION ( 'NONE',  ( -2.269747459788999852E-13, -2.220446049250325308E-15, -1.000000000000000000 ) ) ;
#14507=CARTESIAN_POINT ( 'NONE',  ( -14.00000000144900092, -4.350228928435750042, -6.749999999996870059 ) ) ;
#14562=ORIENTED_EDGE ( 'NONE', *, *, #18926, .T. ) ;
#14619=VERTEX_POINT ( 'NONE', #2515 ) ;
#14620=CARTESIAN_POINT ( 'NONE',  ( -14.98746859792130159, 26.70208920133150343, -6.749999999996710187 ) ) ;
#14660=AXIS2_PLACEMENT_3D ( 'NONE', #9806, #11717, #4210 ) ;
#14663=CARTESIAN_POINT ( 'NONE',  ( -20.00000000397459843, 22.95208919257349933, -7.999999999995569766 ) ) ;
#14705=AXIS2_PLACEMENT_3D ( 'NONE', #11855, #6735, #1126 ) ;
#14746=LINE ( 'NONE', #11086, #21921 ) ;
#14787=DIRECTION ( 'NONE',  ( -3.332943903795901177E-07, 0.000000000000000000, 0.9999999999999444888 ) ) ;
#14836=DIRECTION ( 'NONE',  ( 1.000000000000000000, 9.249025156865542385E-11, -2.269596547736322531E-13 ) ) ;
#14851=LINE ( 'NONE', #11436, #9355 ) ;
#14894=LINE ( 'NONE', #2437, #2049 ) ;
#14913=PLANE ( 'NONE',  #18615 ) ;
#14917=DIRECTION ( 'NONE',  ( 0.7806762821593219437, -0.6249356306643899517, -1.755540157688528780E-13 ) ) ;
#14943=CIRCLE ( 'NONE', #4704, 2.500000000000000444 ) ;
#14992=CYLINDRICAL_SURFACE ( 'NONE', #6962, 2.500000000000000444 ) ;
#15004=( NAMED_UNIT ( * ) PLANE_ANGLE_UNIT ( ) SI_UNIT ( $, .RADIAN. ) );
#15045=CARTESIAN_POINT ( 'NONE',  ( -14.00000000397430000, 22.95208919312840123, -6.749999999996930455 ) ) ;
#15052=ORIENTED_EDGE ( 'NONE', *, *, #9574, .T. ) ;
#15079=ORIENTED_EDGE ( 'NONE', *, *, #19251, .F. ) ;
#15124=FACE_BOUND ( 'NONE', #7877, .T. ) ;
#15193=ORIENTED_EDGE ( 'NONE', *, *, #17934, .F. ) ;
#15194=DIRECTION ( 'NONE',  ( 0.7806762821593219437, -0.6249356306643899517, -1.759009604640482394E-13 ) ) ;
#15267=CARTESIAN_POINT ( 'NONE',  ( -20.00000000397400157, 22.95208919257349933, -5.499999999995569766 ) ) ;
#15293=ORIENTED_EDGE ( 'NONE', *, *, #5223, .T. ) ;
#15311=AXIS2_PLACEMENT_3D ( 'NONE', #5575, #9149, #2372 ) ;
#15318=EDGE_LOOP ( 'NONE', ( #21129, #19413, #2133, #10193 ) ) ;
#15451=DIRECTION ( 'NONE',  ( 0.9949874374308176339, 0.09999999677427344469, -2.262079412673755946E-13 ) ) ;
#15557=ADVANCED_FACE ( 'NONE', ( #21576 ), #5313, .T. ) ;
#15634=CARTESIAN_POINT ( 'NONE',  ( -14.98746859792100139, 26.70208920133150343, -5.499999999996710187 ) ) ;
#15700=CARTESIAN_POINT ( 'NONE',  ( -22.50000000397459843, 22.95208917591821773, -7.999999999995002220 ) ) ;
#15775=CYLINDRICAL_SURFACE ( 'NONE', #7420, 2.499999999999998668 ) ;
#15817=ORIENTED_EDGE ( 'NONE', *, *, #18926, .F. ) ;
#15826=CARTESIAN_POINT ( 'NONE',  ( -20.00000000397400157, 22.95208919257349933, -5.499999999995569766 ) ) ;
#15850=AXIS2_PLACEMENT_3D ( 'NONE', #5404, #9321, #3731 ) ;
#15868=ADVANCED_FACE ( 'NONE', ( #21297 ), #23183, .F. ) ;
#15915=CARTESIAN_POINT ( 'NONE',  ( -25.01253141238839817, 26.70208918381559826, -7.999999999994430233 ) ) ;
#15920=LINE ( 'NONE', #3101, #7130 ) ;
#15954=VERTEX_POINT ( 'NONE', #7522 ) ;
#16020=LINE ( 'NONE', #12813, #2392 ) ;
#16050=EDGE_LOOP ( 'NONE', ( #21799, #18534, #13854, #5658 ) ) ;
#16091=EDGE_CURVE ( 'NONE', #20507, #10293, #5722, .T. ) ;
#16102=CARTESIAN_POINT ( 'NONE',  ( -22.52506283708769885, 28.95208917575130414, -7.999999999995009325 ) ) ;
#16192=VERTEX_POINT ( 'NONE', #9781 ) ;
#16210=DIRECTION ( 'NONE',  ( -0.8823529412199658806, 0.4705882352125641543, 1.991462550421374292E-13 ) ) ;
#16256=DIRECTION ( 'NONE',  ( -2.350988701644575146E-39, 1.000000000000000000, -9.249330715586770885E-11 ) ) ;
#16322=DIRECTION ( 'NONE',  ( 1.000000000000000000, 9.249025156865542385E-11, -2.269596547736322531E-13 ) ) ;
#16355=AXIS2_PLACEMENT_3D ( 'NONE', #13993, #1287, #4968 ) ;
#16390=LINE ( 'NONE', #14620, #9488 ) ;
#16422=CARTESIAN_POINT ( 'NONE',  ( -20.00000000397400157, 22.95208919257349933, -5.499999999995569766 ) ) ;
#16437=CARTESIAN_POINT ( 'NONE',  ( -14.54830929662900019, 0.3367883020382110293, -7.999999999996749267 ) ) ;
#16466=VERTEX_POINT ( 'NONE', #23279 ) ;
#16508=LINE ( 'NONE', #14507, #2036 ) ;
#16587=DIRECTION ( 'NONE',  ( 2.269747459788994803E-13, 2.220446049250310320E-15, 1.000000000000000000 ) ) ;
#16637=DIRECTION ( 'NONE',  ( -1.000000000000000000, -6.662111938308250026E-09, 2.269747459936919981E-13 ) ) ;
#16645=DIRECTION ( 'NONE',  ( 0.9949874374308234071, 0.09999999677421649025, -2.262079412673754937E-13 ) ) ;
#16761=AXIS2_PLACEMENT_3D ( 'NONE', #7817, #16587, #23395 ) ;
#16810=ORIENTED_EDGE ( 'NONE', *, *, #17194, .F. ) ;
#16820=AXIS2_PLACEMENT_3D ( 'NONE', #12113, #19334, #19686 ) ;
#16864=VERTEX_POINT ( 'NONE', #12011 ) ;
#16890=ORIENTED_EDGE ( 'NONE', *, *, #22920, .T. ) ;
#16952=CARTESIAN_POINT ( 'NONE',  ( -26.00000000000209610, -20.00000000055539928, -7.999999999994108713 ) ) ;
#16955=DIRECTION ( 'NONE',  ( 2.269747459788990007E-13, 2.220446049250330436E-15, 1.000000000000000000 ) ) ;
#16961=EDGE_CURVE ( 'NONE', #3332, #8528, #14235, .T. ) ;
#17031=CARTESIAN_POINT ( 'NONE',  ( -14.70588235717629821, 25.77561860482770228, -5.499999999996769695 ) ) ;
#17133=EDGE_LOOP ( 'NONE', ( #14562, #20402, #20981, #17609 ) ) ;
#17138=CARTESIAN_POINT ( 'NONE',  ( -25.01253141238790079, 26.70208918381559826, -5.499999999994429345 ) ) ;
#17151=VECTOR ( 'NONE', #14031, 1000.000000000000000 ) ;
#17185=CARTESIAN_POINT ( 'NONE',  ( -14.00000000397460020, 22.95208919312840123, -7.999999999996929567 ) ) ;
#17186=AXIS2_PLACEMENT_3D ( 'NONE', #16422, #21992, #1813 ) ;
#17194=EDGE_CURVE ( 'NONE', #5941, #4383, #9325, .T. ) ;
#17201=CIRCLE ( 'NONE', #5059, 2.499999999999998668 ) ;
#17279=ADVANCED_FACE ( 'NONE', ( #21040 ), #20364, .T. ) ;
#17305=AXIS2_PLACEMENT_3D ( 'NONE', #11361, #3974, #7655 ) ;
#17312=DIRECTION ( 'NONE',  ( 9.248937406224699144E-11, -1.000000000000000000, 2.220446028257580150E-15 ) ) ;
#17360=ORIENTED_EDGE ( 'NONE', *, *, #8984, .F. ) ;
#17367=AXIS2_PLACEMENT_3D ( 'NONE', #5061, #21083, #13962 ) ;
#17383=CARTESIAN_POINT ( 'NONE',  ( -26.00000000397409750, 22.95208919201850151, -5.499999999994199307 ) ) ;
#17418=FACE_OUTER_BOUND ( 'NONE', #18657, .T. ) ;
#17425=EDGE_LOOP ( 'NONE', ( #16810, #17360, #6679, #23318 ) ) ;
#17444=CYLINDRICAL_SURFACE ( 'NONE', #21527, 2.499999999999998668 ) ;
#17445=DIRECTION ( 'NONE',  ( 2.269747459788999852E-13, 2.220446049250470459E-15, 1.000000000000000000 ) ) ;
#17447=CIRCLE ( 'NONE', #1495, 2.500000000000000000 ) ;
#17452=ORIENTED_EDGE ( 'NONE', *, *, #7067, .F. ) ;
#17483=CARTESIAN_POINT ( 'NONE',  ( -20.00000000000180123, -20.00000000000000000, -7.999999999995469402 ) ) ;
#17602=ORIENTED_EDGE ( 'NONE', *, *, #782, .F. ) ;
#17609=ORIENTED_EDGE ( 'NONE', *, *, #449, .F. ) ;
#17612=AXIS2_PLACEMENT_3D ( 'NONE', #160, #273, #13005 ) ;
#17619=ADVANCED_FACE ( 'NONE', ( #1891 ), #11310, .F. ) ;
#17643=EDGE_CURVE ( 'NONE', #18788, #12123, #3939, .T. ) ;
#17644=ORIENTED_EDGE ( 'NONE', *, *, #5363, .T. ) ;
#17662=VECTOR ( 'NONE', #8651, 1000.000000000000000 ) ;
#17681=DIRECTION ( 'NONE',  ( -1.000000000000000000, -6.662112528310618598E-09, 2.269018306577664942E-13 ) ) ;
#17690=ORIENTED_EDGE ( 'NONE', *, *, #6434, .F. ) ;
#17721=ORIENTED_EDGE ( 'NONE', *, *, #8356, .F. ) ;
#17833=DIRECTION ( 'NONE',  ( -6.662112528310618598E-09, 1.000000000000000000, -2.081668171172169697E-15 ) ) ;
#17837=EDGE_CURVE ( 'NONE', #10039, #10837, #14943, .T. ) ;
#17934=EDGE_CURVE ( 'NONE', #16466, #1142, #14199, .T. ) ;
#17959=VERTEX_POINT ( 'NONE', #10465 ) ;
#18014=DIRECTION ( 'NONE',  ( 2.269747459788994803E-13, 2.220446049250480319E-15, 1.000000000000000000 ) ) ;
#18028=AXIS2_PLACEMENT_3D ( 'NONE', #9491, #5922, #6037 ) ;
#18078=DIRECTION ( 'NONE',  ( -1.000000000000000000, -6.662112528310618598E-09, 2.269018306577664942E-13 ) ) ;
#18122=CIRCLE ( 'NONE', #13551, 2.500000000000000444 ) ;
#18160=ORIENTED_EDGE ( 'NONE', *, *, #13071, .T. ) ;
#18210=FACE_OUTER_BOUND ( 'NONE', #7835, .T. ) ;
#18215=DIRECTION ( 'NONE',  ( 2.269747459788994803E-13, 2.220446049250305192E-15, 1.000000000000000000 ) ) ;
#18222=CIRCLE ( 'NONE', #1948, 2.499999999999998668 ) ;
#18257=ORIENTED_EDGE ( 'NONE', *, *, #14164, .F. ) ;
#18261=CARTESIAN_POINT ( 'NONE',  ( -14.00000000000130029, -19.99999999944489915, -5.499999999996829203 ) ) ;
#18292=EDGE_CURVE ( 'NONE', #12006, #8528, #8167, .T. ) ;
#18323=EDGE_LOOP ( 'NONE', ( #19502, #21035, #22987, #13060 ) ) ;
#18359=FACE_OUTER_BOUND ( 'NONE', #20515, .T. ) ;
#18409=FACE_OUTER_BOUND ( 'NONE', #20775, .T. ) ;
#18505=CIRCLE ( 'NONE', #17367, 6.000000000000109246 ) ;
#18519=ORIENTED_EDGE ( 'NONE', *, *, #22296, .T. ) ;
#18534=ORIENTED_EDGE ( 'NONE', *, *, #17194, .T. ) ;
#18615=AXIS2_PLACEMENT_3D ( 'NONE', #3861, #20369, #14787 ) ;
#18619=CARTESIAN_POINT ( 'NONE',  ( -17.47493720815329965, 28.95208920939580111, -5.499999999996149747 ) ) ;
#18657=EDGE_LOOP ( 'NONE', ( #17452, #13487, #590, #4569 ) ) ;
#18675=EDGE_CURVE ( 'NONE', #1138, #2989, #4655, .T. ) ;
#18697=ORIENTED_EDGE ( 'NONE', *, *, #13435, .F. ) ;
#18749=CARTESIAN_POINT ( 'NONE',  ( -14.00000000144870071, -4.350228928435750042, -5.499999999996869171 ) ) ;
#18762=CARTESIAN_POINT ( 'NONE',  ( -14.00000000000130029, -19.99999999944489915, -5.499999999996829203 ) ) ;
#18788=VERTEX_POINT ( 'NONE', #17031 ) ;
#18795=CIRCLE ( 'NONE', #7406, 2.499999999999998668 ) ;
#18909=AXIS2_PLACEMENT_3D ( 'NONE', #4551, #3123, #18933 ) ;
#18926=EDGE_CURVE ( 'NONE', #23261, #10381, #9198, .T. ) ;
#18933=DIRECTION ( 'NONE',  ( 0.9949874374308176339, 0.09999999677427344469, -2.262079412673755946E-13 ) ) ;
#18944=DIRECTION ( 'NONE',  ( -2.269747459788999852E-13, -2.220446049250325308E-15, -1.000000000000000000 ) ) ;
#18954=DIRECTION ( 'NONE',  ( -2.269747459788990007E-13, -2.220446049250330436E-15, -1.000000000000000000 ) ) ;
#18976=EDGE_CURVE ( 'NONE', #14619, #13456, #19184, .T. ) ;
#19074=FACE_OUTER_BOUND ( 'NONE', #11943, .T. ) ;
#19094=AXIS2_PLACEMENT_3D ( 'NONE', #19994, #18215, #16645 ) ;
#19153=DIRECTION ( 'NONE',  ( 2.269747459788999852E-13, 2.220446049250325308E-15, 1.000000000000000000 ) ) ;
#19184=LINE ( 'NONE', #22847, #13370 ) ;
#19250=ADVANCED_FACE ( 'NONE', ( #18210 ), #1926, .T. ) ;
#19251=EDGE_CURVE ( 'NONE', #1462, #22163, #2780, .T. ) ;
#19267=CARTESIAN_POINT ( 'NONE',  ( -14.54830929633980041, -2.787889851644890005, -6.749999999996740385 ) ) ;
#19286=CARTESIAN_POINT ( 'NONE',  ( -26.00000000397439948, 22.95208919201850151, -6.749999999994200195 ) ) ;
#19291=ORIENTED_EDGE ( 'NONE', *, *, #3592, .T. ) ;
#19306=ADVANCED_FACE ( 'NONE', ( #7071 ), #14992, .T. ) ;
#19334=DIRECTION ( 'NONE',  ( -2.269747459788994803E-13, -2.220446049250305192E-15, -1.000000000000000000 ) ) ;
#19382=PRODUCT_DEFINITION ( 'UNKNOWN', '', #11856, #3038 ) ;
#19413=ORIENTED_EDGE ( 'NONE', *, *, #19537, .F. ) ;
#19477=AXIS2_PLACEMENT_3D ( 'NONE', #23050, #6803, #12282 ) ;
#19491=ORIENTED_EDGE ( 'NONE', *, *, #4870, .T. ) ;
#19502=ORIENTED_EDGE ( 'NONE', *, *, #18292, .T. ) ;
#19537=EDGE_CURVE ( 'NONE', #13627, #22148, #11537, .T. ) ;
#19559=EDGE_LOOP ( 'NONE', ( #16890, #17690, #9252, #4372 ) ) ;
#19640=EDGE_CURVE ( 'NONE', #10837, #1739, #2021, .T. ) ;
#19648=ORIENTED_EDGE ( 'NONE', *, *, #19251, .T. ) ;
#19659=DIRECTION ( 'NONE',  ( -1.000000000000000000, -6.662112528310618598E-09, 2.269018306577664942E-13 ) ) ;
#19686=DIRECTION ( 'NONE',  ( 0.9949874374308234071, 0.09999999677421649025, -2.262079412673754937E-13 ) ) ;
#19707=ADVANCED_FACE ( 'NONE', ( #5358 ), #22052, .F. ) ;
#19777=FACE_OUTER_BOUND ( 'NONE', #9278, .T. ) ;
#19787=CARTESIAN_POINT ( 'NONE',  ( -16.50000000144930112, -4.350228928667009498, -7.999999999996299849 ) ) ;
#19884=CARTESIAN_POINT ( 'NONE',  ( -17.50000000397400157, 22.95208920922877738, -5.499999999996137312 ) ) ;
#19906=DIRECTION ( 'NONE',  ( -0.8823529412199823119, 0.4705882352125332901, 1.992040791580033901E-13 ) ) ;
#19931=VERTEX_POINT ( 'NONE', #16952 ) ;
#19994=CARTESIAN_POINT ( 'NONE',  ( -12.50000000434390124, 26.95208919326699970, -5.499999999997269740 ) ) ;
#20009=CARTESIAN_POINT ( 'NONE',  ( -22.50000000000130029, -20.00000001665528160, -5.499999999994901856 ) ) ;
#20068=DIRECTION ( 'NONE',  ( 2.269747459789000104E-13, 2.220446049250330436E-15, 1.000000000000000000 ) ) ;
#20127=DIRECTION ( 'NONE',  ( 2.269747459788994803E-13, 2.220446049250330436E-15, 1.000000000000000000 ) ) ;
#20173=ORIENTED_EDGE ( 'NONE', *, *, #7243, .T. ) ;
#20192=ORIENTED_EDGE ( 'NONE', *, *, #17643, .T. ) ;
#20198=CARTESIAN_POINT ( 'NONE',  ( -16.50000000202679828, 1.899127378699200008, -5.499999999996309619 ) ) ;
#20257=DIRECTION ( 'NONE',  ( -1.000000000000000000, -9.259491321837100239E-11, 2.269596547736281384E-13 ) ) ;
#20320=CARTESIAN_POINT ( 'NONE',  ( -22.52506282043239594, 26.45208917575140006, -7.999999999994998667 ) ) ;
#20332=ADVANCED_FACE ( 'NONE', ( #19074 ), #4460, .T. ) ;
#20345=ORIENTED_EDGE ( 'NONE', *, *, #9988, .F. ) ;
#20364=CYLINDRICAL_SURFACE ( 'NONE', #14167, 6.000000000000109246 ) ;
#20367=ORIENTED_EDGE ( 'NONE', *, *, #17934, .T. ) ;
#20369=DIRECTION ( 'NONE',  ( -6.662111938308250854E-09, 1.000000000000000000, -2.220444537119161047E-15 ) ) ;
#20391=CIRCLE ( 'NONE', #10179, 2.499999999999998668 ) ;
#20402=ORIENTED_EDGE ( 'NONE', *, *, #4906, .F. ) ;
#20407=ORIENTED_EDGE ( 'NONE', *, *, #19537, .T. ) ;
#20461=ORIENTED_EDGE ( 'NONE', *, *, #22749, .F. ) ;
#20485=VECTOR ( 'NONE', #3946, 1000.000000000000000 ) ;
#20507=VERTEX_POINT ( 'NONE', #8612 ) ;
#20515=EDGE_LOOP ( 'NONE', ( #3385, #20345, #22979, #13816 ) ) ;
#20574=CARTESIAN_POINT ( 'NONE',  ( -14.00000000000150102, -19.99999999944489915, -6.749999999996830091 ) ) ;
#20584=CARTESIAN_POINT ( 'NONE',  ( -14.98746859792150055, 26.70208920133150343, -7.999999999996709299 ) ) ;
#20723=EDGE_CURVE ( 'NONE', #10381, #18788, #3536, .T. ) ;
#20734=LINE ( 'NONE', #18619, #4113 ) ;
#20771=FACE_OUTER_BOUND ( 'NONE', #13395, .T. ) ;
#20772=DIRECTION ( 'NONE',  ( -2.269747459788994803E-13, -2.220446049250605354E-15, -1.000000000000000000 ) ) ;
#20775=EDGE_LOOP ( 'NONE', ( #17644, #2130, #10258, #19291 ) ) ;
#20806=ORIENTED_EDGE ( 'NONE', *, *, #11257, .F. ) ;
#20820=FACE_OUTER_BOUND ( 'NONE', #17133, .T. ) ;
#20833=DIRECTION ( 'NONE',  ( 0.9949874374308176339, 0.09999999677427344469, -2.262079412673755946E-13 ) ) ;
#20851=VERTEX_POINT ( 'NONE', #20584 ) ;
#20870=VECTOR ( 'NONE', #21668, 1000.000000000000000 ) ;
#20888=DIRECTION ( 'NONE',  ( -0.8823529412199658806, 0.4705882352125641543, 1.991462550421374292E-13 ) ) ;
#20981=ORIENTED_EDGE ( 'NONE', *, *, #11346, .T. ) ;
#21007=DIRECTION ( 'NONE',  ( -2.269747459788990007E-13, -2.220446049250330436E-15, -1.000000000000000000 ) ) ;
#21035=ORIENTED_EDGE ( 'NONE', *, *, #16961, .F. ) ;
#21040=FACE_OUTER_BOUND ( 'NONE', #2552, .T. ) ;
#21043=LINE ( 'NONE', #19267, #17151 ) ;
#21083=DIRECTION ( 'NONE',  ( -2.269747459788994803E-13, -2.220446049250330436E-15, -1.000000000000000000 ) ) ;
#21106=FACE_OUTER_BOUND ( 'NONE', #17425, .T. ) ;
#21129=ORIENTED_EDGE ( 'NONE', *, *, #23264, .F. ) ;
#21165=LINE ( 'NONE', #3117, #1797 ) ;
#21221=AXIS2_PLACEMENT_3D ( 'NONE', #20198, #337, #15194 ) ;
#21235=DIRECTION ( 'NONE',  ( -2.269747459788990007E-13, -2.220446049250330436E-15, -1.000000000000000000 ) ) ;
#21236=AXIS2_PLACEMENT_3D ( 'NONE', #4862, #21235, #3078 ) ;
#21297=FACE_OUTER_BOUND ( 'NONE', #22289, .T. ) ;
#21318=CARTESIAN_POINT ( 'NONE',  ( -20.00000000000190070, -20.00000000000000000, -7.999999999995469402 ) ) ;
#21349=CARTESIAN_POINT ( 'NONE',  ( -17.50000000000149925, -19.99999998334472195, -6.749999999996036948 ) ) ;
#21355=EDGE_CURVE ( 'NONE', #11278, #17959, #14851, .T. ) ;
#21396=VECTOR ( 'NONE', #8598, 1000.000000000000000 ) ;
#21484=VECTOR ( 'NONE', #22594, 1000.000000000000000 ) ;
#21527=AXIS2_PLACEMENT_3D ( 'NONE', #8082, #1161, #22905 ) ;
#21576=FACE_OUTER_BOUND ( 'NONE', #18323, .T. ) ;
#21578=EDGE_LOOP ( 'NONE', ( #19648, #20806, #9255, #22745 ) ) ;
#21602=ORIENTED_EDGE ( 'NONE', *, *, #4721, .F. ) ;
#21668=DIRECTION ( 'NONE',  ( 9.249330715586770885E-11, -1.000000000000000000, 2.220446028256680454E-15 ) ) ;
#21709=DIRECTION ( 'NONE',  ( 2.269747459789000104E-13, 2.220446049250330436E-15, 1.000000000000000000 ) ) ;
#21744=DIRECTION ( 'NONE',  ( 2.269747459789000104E-13, 2.220446049250330436E-15, 1.000000000000000000 ) ) ;
#21751=CARTESIAN_POINT ( 'NONE',  ( -26.00000000397469790, 22.95208919201850151, -7.999999999994199307 ) ) ;
#21799=ORIENTED_EDGE ( 'NONE', *, *, #12586, .F. ) ;
#21876=CARTESIAN_POINT ( 'NONE',  ( -26.00000000000179767, -20.00000000055539928, -6.749999999994109601 ) ) ;
#21904=ORIENTED_EDGE ( 'NONE', *, *, #9988, .T. ) ;
#21921=VECTOR ( 'NONE', #7744, 1000.000000000000000 ) ;
#21949=CARTESIAN_POINT ( 'NONE',  ( -20.00000000397400157, 22.95208919257349933, -5.499999999995569766 ) ) ;
#21992=DIRECTION ( 'NONE',  ( -2.269747459788994803E-13, -2.220446049250470459E-15, -1.000000000000000000 ) ) ;
#22022=CARTESIAN_POINT ( 'NONE',  ( -14.00000000202680006, 1.899127378930359988, -5.499999999996879829 ) ) ;
#22037=DIRECTION ( 'NONE',  ( 2.269747459789000104E-13, 2.220446049250330436E-15, 1.000000000000000000 ) ) ;
#22039=LINE ( 'NONE', #23380, #11428 ) ;
#22052=CYLINDRICAL_SURFACE ( 'NONE', #16761, 2.500000000000001776 ) ;
#22090=DIRECTION ( 'NONE',  ( 2.269747459788990007E-13, 2.220446049250330436E-15, 1.000000000000000000 ) ) ;
#22148=VERTEX_POINT ( 'NONE', #11731 ) ;
#22163=VERTEX_POINT ( 'NONE', #6473 ) ;
#22177=EDGE_CURVE ( 'NONE', #4383, #17959, #23027, .T. ) ;
#22178=CIRCLE ( 'NONE', #18028, 2.500000000000000444 ) ;
#22231=CARTESIAN_POINT ( 'NONE',  ( -14.00000000144930112, -4.350228928435750042, -7.999999999996869171 ) ) ;
#22255=CARTESIAN_POINT ( 'NONE',  ( -16.50000000202710027, 1.899127378699190016, -6.749999999996310507 ) ) ;
#22289=EDGE_LOOP ( 'NONE', ( #20367, #21602, #18519, #5548 ) ) ;
#22296=EDGE_CURVE ( 'NONE', #2989, #8934, #9779, .T. ) ;
#22364=CARTESIAN_POINT ( 'NONE',  ( -20.00000000000170175, -20.00000000000000000, -6.749999999995469402 ) ) ;
#22436=ORIENTED_EDGE ( 'NONE', *, *, #236, .F. ) ;
#22457=VECTOR ( 'NONE', #16637, 1000.000000000000000 ) ;
#22470=ORIENTED_EDGE ( 'NONE', *, *, #12586, .T. ) ;
#22471=DIRECTION ( 'NONE',  ( 1.000000000000000000, 9.250482324585361611E-11, -2.269018306577663175E-13 ) ) ;
#22594=DIRECTION ( 'NONE',  ( -9.248937406224699144E-11, 1.000000000000000000, -2.220446028257580150E-15 ) ) ;
#22602=VERTEX_POINT ( 'NONE', #17138 ) ;
#22698=CLOSED_SHELL ( 'NONE', ( #17619, #13696, #8797, #23251, #2547, #12619, #19707, #13784, #2214, #20332, #15868, #19306, #15557, #17279, #19250, #3805, #8978, #11846, #5458, #23170 ) ) ;
#22718=PRODUCT_DEFINITION_SHAPE ( 'NONE', 'NONE',  #19382 ) ;
#22745=ORIENTED_EDGE ( 'NONE', *, *, #9260, .T. ) ;
#22749=EDGE_CURVE ( 'NONE', #15954, #1462, #21165, .T. ) ;
#22785=CIRCLE ( 'NONE', #2313, 6.000000000000000000 ) ;
#22807=DIRECTION ( 'NONE',  ( 2.269747459788994803E-13, 2.220446049250330436E-15, 1.000000000000000000 ) ) ;
#22847=CARTESIAN_POINT ( 'NONE',  ( -14.00000000202730099, 1.899127378930349996, -7.999999999996879829 ) ) ;
#22887=CIRCLE ( 'NONE', #16820, 2.500000000000001776 ) ;
#22905=DIRECTION ( 'NONE',  ( -6.662112528310618598E-09, 1.000000000000000000, -2.081668171172169697E-15 ) ) ;
#22920=EDGE_CURVE ( 'NONE', #1142, #12006, #22178, .T. ) ;
#22937=DIRECTION ( 'NONE',  ( -1.000000000000000000, -6.662112528310618598E-09, 2.269018306577664942E-13 ) ) ;
#22946=AXIS2_PLACEMENT_3D ( 'NONE', #6645, #13634, #11884 ) ;
#22979=ORIENTED_EDGE ( 'NONE', *, *, #17837, .T. ) ;
#22987=ORIENTED_EDGE ( 'NONE', *, *, #14164, .T. ) ;
#23027=CIRCLE ( 'NONE', #11689, 2.499999999999998668 ) ;
#23050=CARTESIAN_POINT ( 'NONE',  ( -20.00000000397459843, 22.95208919257349933, -7.999999999995569766 ) ) ;
#23055=DIRECTION ( 'NONE',  ( -2.269747459788990007E-13, -2.220446049250330436E-15, -1.000000000000000000 ) ) ;
#23098=EDGE_LOOP ( 'NONE', ( #22436, #5859, #2172, #17721, #13881, #7761, #17602, #12275, #7033, #18257, #1507, #1518, #191, #10697 ) ) ;
#23106=CARTESIAN_POINT ( 'NONE',  ( -17.47493720815329965, 28.95208920939580111, -5.499999999996149747 ) ) ;
#23108=AXIS2_PLACEMENT_3D ( 'NONE', #12834, #14498, #17833 ) ;
#23170=ADVANCED_FACE ( 'NONE', ( #2944, #8416, #4611 ), #10093, .T. ) ;
#23183=CYLINDRICAL_SURFACE ( 'NONE', #9958, 2.500000000000000444 ) ;
#23251=ADVANCED_FACE ( 'NONE', ( #21106 ), #15775, .F. ) ;
#23260=VECTOR ( 'NONE', #17312, 1000.000000000000000 ) ;
#23261=VERTEX_POINT ( 'NONE', #23106 ) ;
#23264=EDGE_CURVE ( 'NONE', #22148, #16864, #10331, .T. ) ;
#23268=AXIS2_PLACEMENT_3D ( 'NONE', #10305, #8391, #19659 ) ;
#23272=VERTEX_POINT ( 'NONE', #8543 ) ;
#23279=CARTESIAN_POINT ( 'NONE',  ( -14.54830929662849925, 0.3367883020382200221, -5.499999999996749267 ) ) ;
#23318=ORIENTED_EDGE ( 'NONE', *, *, #22177, .F. ) ;
#23380=CARTESIAN_POINT ( 'NONE',  ( -25.01253141238809974, 26.70208918381559826, -6.749999999994429345 ) ) ;
#23386=VECTOR ( 'NONE', #14398, 1000.000000000000000 ) ;
#23393=EDGE_LOOP ( 'NONE', ( #15817, #18697, #11982, #13804, #15079, #20461, #7594, #3767, #1769, #15193, #1420, #787, #2478, #11068 ) ) ;
#23395=DIRECTION ( 'NONE',  ( 0.9949874374308234071, 0.09999999677421649025, -2.262079412673754937E-13 ) ) ;
#23424=ORIENTED_EDGE ( 'NONE', *, *, #10531, .T. ) ;
#23433=DIRECTION ( 'NONE',  ( -2.269747459788999852E-13, -2.220446049250470459E-15, -1.000000000000000000 ) ) ;
#23452=VERTEX_POINT ( 'NONE', #10918 ) ;
#23543=COLOUR_RGB('Light Gray', 0.72549020, 0.75294118, 0.79215686);
#23544=FILL_AREA_STYLE_COLOUR('',#23543);
#23545=FILL_AREA_STYLE('',(#23544));
#23546=SURFACE_STYLE_FILL_AREA(#23545);
#23547=SURFACE_SIDE_STYLE('',(#23546));
#23548=SURFACE_STYLE_USAGE(.BOTH.,#23547);
#23549=PRESENTATION_STYLE_ASSIGNMENT((#23548));
#23575=STYLED_ITEM('',(#23549),#9367);
#23576=MECHANICAL_DESIGN_GEOMETRIC_PRESENTATION_REPRESENTATION('',(#23575),#1734);
ENDSEC;
END-ISO-10303-21;
